ISO-10303-21;
HEADER;
/* Generated by software containing ST-Developer
 * from STEP Tools, Inc. (www.steptools.com) 
 */

FILE_DESCRIPTION(
/* description */ ('Counterbalanced vertical column'),
/* implementation_level */ '2;1');

FILE_NAME(
/* name */ 'Cap Screw - M5x20.step',
/* time_stamp */ '2026-10-29T16:47:22-07:00',
/* author */ (''),
/* organization */ (''),
/* preprocessor_version */ 'ST-DEVELOPER v20.2',
/* originating_system */ 'Autodesk Translation Framework v15.17.0.0',
/* authorisation */ '');

FILE_SCHEMA (('AUTOMOTIVE_DESIGN { 1 0 10303 214 3 1 1 }'));
ENDSEC;

DATA;
#10=MECHANICAL_DESIGN_GEOMETRIC_PRESENTATION_REPRESENTATION('',(#370),#15040);
#250=CONICAL_SURFACE('',#7876,0.4,0.785398163397448);
#251=CONICAL_SURFACE('',#7880,0.41,0.785398163397448);
#252=CONICAL_SURFACE('',#7884,0.26,0.463647609000806);
#253=CONICAL_SURFACE('',#7888,0.225,0.785398163397448);
#263=ORIENTED_CLOSED_SHELL('',*,#7095,.F.);
#267=BREP_WITH_VOIDS('Body1',#7094,(#263));
#300=SHAPE_REPRESENTATION_RELATIONSHIP('SRR','None',#15204,#335);
#335=ADVANCED_BREP_SHAPE_REPRESENTATION('',(#267),#15023);
#370=STYLED_ITEM('',(#15464),#267);
#494=FACE_BOUND('',#1541,.T.);
#695=PLANE('',#7874);
#696=PLANE('',#7882);
#697=PLANE('',#7890);
#698=PLANE('',#7891);
#699=PLANE('',#7892);
#700=PLANE('',#7893);
#701=PLANE('',#7894);
#702=PLANE('',#7895);
#703=PLANE('',#7896);
#704=PLANE('',#7897);
#705=PLANE('',#7898);
#1053=FACE_OUTER_BOUND('',#1536,.T.);
#1054=FACE_OUTER_BOUND('',#1537,.T.);
#1055=FACE_OUTER_BOUND('',#1538,.T.);
#1056=FACE_OUTER_BOUND('',#1539,.T.);
#1057=FACE_OUTER_BOUND('',#1540,.T.);
#1058=FACE_OUTER_BOUND('',#1542,.T.);
#1059=FACE_OUTER_BOUND('',#1543,.T.);
#1060=FACE_OUTER_BOUND('',#1544,.T.);
#1061=FACE_OUTER_BOUND('',#1545,.T.);
#1062=FACE_OUTER_BOUND('',#1546,.T.);
#1063=FACE_OUTER_BOUND('',#1547,.T.);
#1064=FACE_OUTER_BOUND('',#1548,.T.);
#1065=FACE_OUTER_BOUND('',#1549,.T.);
#1066=FACE_OUTER_BOUND('',#1550,.T.);
#1067=FACE_OUTER_BOUND('',#1551,.T.);
#1068=FACE_OUTER_BOUND('',#1552,.T.);
#1069=FACE_OUTER_BOUND('',#1553,.T.);
#1536=EDGE_LOOP('',(#5772));
#1537=EDGE_LOOP('',(#5773,#5774,#5775,#5776));
#1538=EDGE_LOOP('',(#5777,#5778,#5779,#5780));
#1539=EDGE_LOOP('',(#5781,#5782,#5783,#5784));
#1540=EDGE_LOOP('',(#5785));
#1541=EDGE_LOOP('',(#5786));
#1542=EDGE_LOOP('',(#5787,#5788,#5789,#5790));
#1543=EDGE_LOOP('',(#5791,#5792,#5793,#5794));
#1544=EDGE_LOOP('',(#5795,#5796,#5797,#5798));
#1545=EDGE_LOOP('',(#5799));
#1546=EDGE_LOOP('',(#5800,#5801,#5802,#5803));
#1547=EDGE_LOOP('',(#5804,#5805,#5806,#5807));
#1548=EDGE_LOOP('',(#5808,#5809,#5810,#5811));
#1549=EDGE_LOOP('',(#5812,#5813,#5814,#5815));
#1550=EDGE_LOOP('',(#5816,#5817,#5818,#5819));
#1551=EDGE_LOOP('',(#5820,#5821,#5822,#5823));
#1552=EDGE_LOOP('',(#5824,#5825,#5826,#5827,#5828,#5829));
#1553=EDGE_LOOP('',(#5830,#5831,#5832,#5833,#5834,#5835));
#2115=LINE('',#14051,#2786);
#2116=LINE('',#14055,#2787);
#2117=LINE('',#14059,#2788);
#2118=LINE('',#14066,#2789);
#2119=LINE('',#14070,#2790);
#2120=LINE('',#14074,#2791);
#2121=LINE('',#14079,#2792);
#2122=LINE('',#14081,#2793);
#2123=LINE('',#14083,#2794);
#2124=LINE('',#14084,#2795);
#2125=LINE('',#14087,#2796);
#2126=LINE('',#14089,#2797);
#2127=LINE('',#14090,#2798);
#2128=LINE('',#14093,#2799);
#2129=LINE('',#14095,#2800);
#2130=LINE('',#14096,#2801);
#2131=LINE('',#14099,#2802);
#2132=LINE('',#14101,#2803);
#2133=LINE('',#14102,#2804);
#2134=LINE('',#14105,#2805);
#2135=LINE('',#14107,#2806);
#2136=LINE('',#14108,#2807);
#2137=LINE('',#14110,#2808);
#2138=LINE('',#14111,#2809);
#2786=VECTOR('',#9345,0.4);
#2787=VECTOR('',#9350,0.425);
#2788=VECTOR('',#9355,0.41);
#2789=VECTOR('',#9364,0.26);
#2790=VECTOR('',#9369,0.25);
#2791=VECTOR('',#9374,0.225);
#2792=VECTOR('',#9379,1.);
#2793=VECTOR('',#9380,1.);
#2794=VECTOR('',#9381,1.);
#2795=VECTOR('',#9382,1.);
#2796=VECTOR('',#9385,1.);
#2797=VECTOR('',#9386,1.);
#2798=VECTOR('',#9387,1.);
#2799=VECTOR('',#9390,1.);
#2800=VECTOR('',#9391,1.);
#2801=VECTOR('',#9392,1.);
#2802=VECTOR('',#9395,1.);
#2803=VECTOR('',#9396,1.);
#2804=VECTOR('',#9397,1.);
#2805=VECTOR('',#9400,1.);
#2806=VECTOR('',#9401,1.);
#2807=VECTOR('',#9402,1.);
#2808=VECTOR('',#9405,1.);
#2809=VECTOR('',#9406,1.);
#3214=CIRCLE('',#7875,0.375);
#3215=CIRCLE('',#7877,0.425);
#3216=CIRCLE('',#7879,0.425);
#3217=CIRCLE('',#7881,0.395);
#3218=CIRCLE('',#7883,0.27);
#3219=CIRCLE('',#7885,0.24505);
#3220=CIRCLE('',#7887,0.24505);
#3221=CIRCLE('',#7889,0.2);
#3633=VERTEX_POINT('',#14046);
#3634=VERTEX_POINT('',#14049);
#3635=VERTEX_POINT('',#14053);
#3636=VERTEX_POINT('',#14057);
#3637=VERTEX_POINT('',#14061);
#3638=VERTEX_POINT('',#14064);
#3639=VERTEX_POINT('',#14068);
#3640=VERTEX_POINT('',#14072);
#3641=VERTEX_POINT('',#14077);
#3642=VERTEX_POINT('',#14078);
#3643=VERTEX_POINT('',#14080);
#3644=VERTEX_POINT('',#14082);
#3645=VERTEX_POINT('',#14086);
#3646=VERTEX_POINT('',#14088);
#3647=VERTEX_POINT('',#14092);
#3648=VERTEX_POINT('',#14094);
#3649=VERTEX_POINT('',#14098);
#3650=VERTEX_POINT('',#14100);
#3651=VERTEX_POINT('',#14104);
#3652=VERTEX_POINT('',#14106);
#4387=EDGE_CURVE('',#3633,#3633,#3214,.T.);
#4388=EDGE_CURVE('',#3634,#3634,#3215,.T.);
#4389=EDGE_CURVE('',#3634,#3633,#2115,.T.);
#4390=EDGE_CURVE('',#3635,#3635,#3216,.T.);
#4391=EDGE_CURVE('',#3635,#3634,#2116,.T.);
#4392=EDGE_CURVE('',#3636,#3636,#3217,.T.);
#4393=EDGE_CURVE('',#3636,#3635,#2117,.T.);
#4394=EDGE_CURVE('',#3637,#3637,#3218,.T.);
#4395=EDGE_CURVE('',#3638,#3638,#3219,.F.);
#4396=EDGE_CURVE('',#3638,#3637,#2118,.T.);
#4397=EDGE_CURVE('',#3639,#3639,#3220,.F.);
#4398=EDGE_CURVE('',#3639,#3638,#2119,.T.);
#4399=EDGE_CURVE('',#3640,#3640,#3221,.T.);
#4400=EDGE_CURVE('',#3640,#3639,#2120,.T.);
#4401=EDGE_CURVE('',#3641,#3642,#2121,.T.);
#4402=EDGE_CURVE('',#3642,#3643,#2122,.T.);
#4403=EDGE_CURVE('',#3643,#3644,#2123,.T.);
#4404=EDGE_CURVE('',#3641,#3644,#2124,.T.);
#4405=EDGE_CURVE('',#3642,#3645,#2125,.T.);
#4406=EDGE_CURVE('',#3645,#3646,#2126,.T.);
#4407=EDGE_CURVE('',#3646,#3643,#2127,.T.);
#4408=EDGE_CURVE('',#3645,#3647,#2128,.T.);
#4409=EDGE_CURVE('',#3647,#3648,#2129,.T.);
#4410=EDGE_CURVE('',#3648,#3646,#2130,.T.);
#4411=EDGE_CURVE('',#3647,#3649,#2131,.T.);
#4412=EDGE_CURVE('',#3649,#3650,#2132,.T.);
#4413=EDGE_CURVE('',#3650,#3648,#2133,.T.);
#4414=EDGE_CURVE('',#3649,#3651,#2134,.T.);
#4415=EDGE_CURVE('',#3651,#3652,#2135,.T.);
#4416=EDGE_CURVE('',#3652,#3650,#2136,.T.);
#4417=EDGE_CURVE('',#3651,#3641,#2137,.T.);
#4418=EDGE_CURVE('',#3644,#3652,#2138,.T.);
#5772=ORIENTED_EDGE('',*,*,#4387,.F.);
#5773=ORIENTED_EDGE('',*,*,#4388,.F.);
#5774=ORIENTED_EDGE('',*,*,#4389,.T.);
#5775=ORIENTED_EDGE('',*,*,#4387,.T.);
#5776=ORIENTED_EDGE('',*,*,#4389,.F.);
#5777=ORIENTED_EDGE('',*,*,#4390,.F.);
#5778=ORIENTED_EDGE('',*,*,#4391,.T.);
#5779=ORIENTED_EDGE('',*,*,#4388,.T.);
#5780=ORIENTED_EDGE('',*,*,#4391,.F.);
#5781=ORIENTED_EDGE('',*,*,#4392,.F.);
#5782=ORIENTED_EDGE('',*,*,#4393,.T.);
#5783=ORIENTED_EDGE('',*,*,#4390,.T.);
#5784=ORIENTED_EDGE('',*,*,#4393,.F.);
#5785=ORIENTED_EDGE('',*,*,#4392,.T.);
#5786=ORIENTED_EDGE('',*,*,#4394,.F.);
#5787=ORIENTED_EDGE('',*,*,#4395,.F.);
#5788=ORIENTED_EDGE('',*,*,#4396,.T.);
#5789=ORIENTED_EDGE('',*,*,#4394,.T.);
#5790=ORIENTED_EDGE('',*,*,#4396,.F.);
#5791=ORIENTED_EDGE('',*,*,#4397,.F.);
#5792=ORIENTED_EDGE('',*,*,#4398,.T.);
#5793=ORIENTED_EDGE('',*,*,#4395,.T.);
#5794=ORIENTED_EDGE('',*,*,#4398,.F.);
#5795=ORIENTED_EDGE('',*,*,#4399,.F.);
#5796=ORIENTED_EDGE('',*,*,#4400,.T.);
#5797=ORIENTED_EDGE('',*,*,#4397,.T.);
#5798=ORIENTED_EDGE('',*,*,#4400,.F.);
#5799=ORIENTED_EDGE('',*,*,#4399,.T.);
#5800=ORIENTED_EDGE('',*,*,#4401,.T.);
#5801=ORIENTED_EDGE('',*,*,#4402,.T.);
#5802=ORIENTED_EDGE('',*,*,#4403,.T.);
#5803=ORIENTED_EDGE('',*,*,#4404,.F.);
#5804=ORIENTED_EDGE('',*,*,#4405,.T.);
#5805=ORIENTED_EDGE('',*,*,#4406,.T.);
#5806=ORIENTED_EDGE('',*,*,#4407,.T.);
#5807=ORIENTED_EDGE('',*,*,#4402,.F.);
#5808=ORIENTED_EDGE('',*,*,#4408,.T.);
#5809=ORIENTED_EDGE('',*,*,#4409,.T.);
#5810=ORIENTED_EDGE('',*,*,#4410,.T.);
#5811=ORIENTED_EDGE('',*,*,#4406,.F.);
#5812=ORIENTED_EDGE('',*,*,#4411,.T.);
#5813=ORIENTED_EDGE('',*,*,#4412,.T.);
#5814=ORIENTED_EDGE('',*,*,#4413,.T.);
#5815=ORIENTED_EDGE('',*,*,#4409,.F.);
#5816=ORIENTED_EDGE('',*,*,#4414,.T.);
#5817=ORIENTED_EDGE('',*,*,#4415,.T.);
#5818=ORIENTED_EDGE('',*,*,#4416,.T.);
#5819=ORIENTED_EDGE('',*,*,#4412,.F.);
#5820=ORIENTED_EDGE('',*,*,#4417,.T.);
#5821=ORIENTED_EDGE('',*,*,#4404,.T.);
#5822=ORIENTED_EDGE('',*,*,#4418,.T.);
#5823=ORIENTED_EDGE('',*,*,#4415,.F.);
#5824=ORIENTED_EDGE('',*,*,#4417,.F.);
#5825=ORIENTED_EDGE('',*,*,#4414,.F.);
#5826=ORIENTED_EDGE('',*,*,#4411,.F.);
#5827=ORIENTED_EDGE('',*,*,#4408,.F.);
#5828=ORIENTED_EDGE('',*,*,#4405,.F.);
#5829=ORIENTED_EDGE('',*,*,#4401,.F.);
#5830=ORIENTED_EDGE('',*,*,#4418,.F.);
#5831=ORIENTED_EDGE('',*,*,#4403,.F.);
#5832=ORIENTED_EDGE('',*,*,#4407,.F.);
#5833=ORIENTED_EDGE('',*,*,#4410,.F.);
#5834=ORIENTED_EDGE('',*,*,#4413,.F.);
#5835=ORIENTED_EDGE('',*,*,#4416,.F.);
#6633=CYLINDRICAL_SURFACE('',#7878,0.425);
#6634=CYLINDRICAL_SURFACE('',#7886,0.24505);
#6895=ADVANCED_FACE('',(#1053),#695,.T.);
#6896=ADVANCED_FACE('',(#1054),#250,.T.);
#6897=ADVANCED_FACE('',(#1055),#6633,.T.);
#6898=ADVANCED_FACE('',(#1056),#251,.T.);
#6899=ADVANCED_FACE('',(#1057,#494),#696,.T.);
#6900=ADVANCED_FACE('',(#1058),#252,.T.);
#6901=ADVANCED_FACE('',(#1059),#6634,.T.);
#6902=ADVANCED_FACE('',(#1060),#253,.T.);
#6903=ADVANCED_FACE('',(#1061),#697,.T.);
#6904=ADVANCED_FACE('',(#1062),#698,.F.);
#6905=ADVANCED_FACE('',(#1063),#699,.F.);
#6906=ADVANCED_FACE('',(#1064),#700,.F.);
#6907=ADVANCED_FACE('',(#1065),#701,.F.);
#6908=ADVANCED_FACE('',(#1066),#702,.F.);
#6909=ADVANCED_FACE('',(#1067),#703,.F.);
#6910=ADVANCED_FACE('',(#1068),#704,.F.);
#6911=ADVANCED_FACE('',(#1069),#705,.F.);
#7094=CLOSED_SHELL('',(#6895,#6896,#6897,#6898,#6899,#6900,#6901,#6902,
#6903));
#7095=CLOSED_SHELL('',(#6904,#6905,#6906,#6907,#6908,#6909,#6910,#6911));
#7873=AXIS2_PLACEMENT_3D('',#14044,#9335,#9336);
#7874=AXIS2_PLACEMENT_3D('',#14045,#9337,#9338);
#7875=AXIS2_PLACEMENT_3D('',#14047,#9339,#9340);
#7876=AXIS2_PLACEMENT_3D('',#14048,#9341,#9342);
#7877=AXIS2_PLACEMENT_3D('',#14050,#9343,#9344);
#7878=AXIS2_PLACEMENT_3D('',#14052,#9346,#9347);
#7879=AXIS2_PLACEMENT_3D('',#14054,#9348,#9349);
#7880=AXIS2_PLACEMENT_3D('',#14056,#9351,#9352);
#7881=AXIS2_PLACEMENT_3D('',#14058,#9353,#9354);
#7882=AXIS2_PLACEMENT_3D('',#14060,#9356,#9357);
#7883=AXIS2_PLACEMENT_3D('',#14062,#9358,#9359);
#7884=AXIS2_PLACEMENT_3D('',#14063,#9360,#9361);
#7885=AXIS2_PLACEMENT_3D('',#14065,#9362,#9363);
#7886=AXIS2_PLACEMENT_3D('',#14067,#9365,#9366);
#7887=AXIS2_PLACEMENT_3D('',#14069,#9367,#9368);
#7888=AXIS2_PLACEMENT_3D('',#14071,#9370,#9371);
#7889=AXIS2_PLACEMENT_3D('',#14073,#9372,#9373);
#7890=AXIS2_PLACEMENT_3D('',#14075,#9375,#9376);
#7891=AXIS2_PLACEMENT_3D('',#14076,#9377,#9378);
#7892=AXIS2_PLACEMENT_3D('',#14085,#9383,#9384);
#7893=AXIS2_PLACEMENT_3D('',#14091,#9388,#9389);
#7894=AXIS2_PLACEMENT_3D('',#14097,#9393,#9394);
#7895=AXIS2_PLACEMENT_3D('',#14103,#9398,#9399);
#7896=AXIS2_PLACEMENT_3D('',#14109,#9403,#9404);
#7897=AXIS2_PLACEMENT_3D('',#14112,#9407,#9408);
#7898=AXIS2_PLACEMENT_3D('',#14113,#9409,#9410);
#9335=DIRECTION('axis',(0.,0.,1.));
#9336=DIRECTION('refdir',(1.,0.,0.));
#9337=DIRECTION('center_axis',(0.,1.,0.));
#9338=DIRECTION('ref_axis',(0.,0.,1.));
#9339=DIRECTION('center_axis',(0.,-1.,0.));
#9340=DIRECTION('ref_axis',(1.,0.,0.));
#9341=DIRECTION('center_axis',(0.,-1.,0.));
#9342=DIRECTION('ref_axis',(1.,0.,0.));
#9343=DIRECTION('center_axis',(0.,-1.,0.));
#9344=DIRECTION('ref_axis',(1.,0.,0.));
#9345=DIRECTION('',(0.707106781186548,0.707106781186547,8.65956056235493E-17));
#9346=DIRECTION('center_axis',(0.,-1.,0.));
#9347=DIRECTION('ref_axis',(1.,0.,0.));
#9348=DIRECTION('center_axis',(0.,-1.,0.));
#9349=DIRECTION('ref_axis',(1.,0.,0.));
#9350=DIRECTION('',(0.,1.,0.));
#9351=DIRECTION('center_axis',(0.,1.,0.));
#9352=DIRECTION('ref_axis',(1.,0.,0.));
#9353=DIRECTION('center_axis',(0.,-1.,0.));
#9354=DIRECTION('ref_axis',(1.,0.,0.));
#9355=DIRECTION('',(-0.707106781186547,0.707106781186548,-8.65956056235493E-17));
#9356=DIRECTION('center_axis',(0.,-1.,0.));
#9357=DIRECTION('ref_axis',(0.,0.,-1.));
#9358=DIRECTION('center_axis',(0.,-1.,0.));
#9359=DIRECTION('ref_axis',(1.,0.,0.));
#9360=DIRECTION('center_axis',(0.,1.,0.));
#9361=DIRECTION('ref_axis',(1.,0.,0.));
#9362=DIRECTION('center_axis',(0.,1.,0.));
#9363=DIRECTION('ref_axis',(1.,0.,0.));
#9364=DIRECTION('',(-0.447213595499958,0.894427190999916,-5.47678698264203E-17));
#9365=DIRECTION('center_axis',(0.,-1.,0.));
#9366=DIRECTION('ref_axis',(1.,0.,0.));
#9367=DIRECTION('center_axis',(0.,1.,0.));
#9368=DIRECTION('ref_axis',(1.,0.,0.));
#9369=DIRECTION('',(0.,1.,0.));
#9370=DIRECTION('center_axis',(0.,1.,0.));
#9371=DIRECTION('ref_axis',(1.,0.,0.));
#9372=DIRECTION('center_axis',(0.,-1.,0.));
#9373=DIRECTION('ref_axis',(1.,0.,0.));
#9374=DIRECTION('',(-0.707106781186547,0.707106781186548,-8.65956056235493E-17));
#9375=DIRECTION('center_axis',(0.,-1.,0.));
#9376=DIRECTION('ref_axis',(0.,0.,-1.));
#9377=DIRECTION('center_axis',(0.866025403784439,0.,-0.5));
#9378=DIRECTION('ref_axis',(0.5,0.,0.866025403784439));
#9379=DIRECTION('',(-0.5,0.,-0.866025403784439));
#9380=DIRECTION('',(0.,-1.,0.));
#9381=DIRECTION('',(0.5,0.,0.866025403784439));
#9382=DIRECTION('',(0.,-1.,0.));
#9383=DIRECTION('center_axis',(1.20185167898973E-16,0.,-1.));
#9384=DIRECTION('ref_axis',(1.,0.,1.20185167898973E-16));
#9385=DIRECTION('',(-1.,0.,-1.20185167898973E-16));
#9386=DIRECTION('',(0.,-1.,0.));
#9387=DIRECTION('',(1.,0.,1.20185167898973E-16));
#9388=DIRECTION('center_axis',(-0.866025403784439,0.,-0.5));
#9389=DIRECTION('ref_axis',(0.5,0.,-0.866025403784439));
#9390=DIRECTION('',(-0.5,0.,0.866025403784439));
#9391=DIRECTION('',(0.,-1.,0.));
#9392=DIRECTION('',(0.5,0.,-0.866025403784439));
#9393=DIRECTION('center_axis',(-0.866025403784439,0.,0.5));
#9394=DIRECTION('ref_axis',(-0.5,0.,-0.866025403784439));
#9395=DIRECTION('',(0.5,0.,0.866025403784439));
#9396=DIRECTION('',(0.,-1.,0.));
#9397=DIRECTION('',(-0.5,0.,-0.866025403784439));
#9398=DIRECTION('center_axis',(-2.40370335797945E-16,0.,1.));
#9399=DIRECTION('ref_axis',(-1.,0.,-2.40370335797945E-16));
#9400=DIRECTION('',(1.,0.,2.40370335797945E-16));
#9401=DIRECTION('',(0.,-1.,0.));
#9402=DIRECTION('',(-1.,0.,-2.40370335797945E-16));
#9403=DIRECTION('center_axis',(0.866025403784439,0.,0.5));
#9404=DIRECTION('ref_axis',(-0.5,0.,0.866025403784439));
#9405=DIRECTION('',(0.5,0.,-0.866025403784439));
#9406=DIRECTION('',(-0.5,0.,0.866025403784439));
#9407=DIRECTION('center_axis',(0.,1.,0.));
#9408=DIRECTION('ref_axis',(1.,0.,0.));
#9409=DIRECTION('center_axis',(0.,-1.,0.));
#9410=DIRECTION('ref_axis',(0.,0.,-1.));
#14044=CARTESIAN_POINT('',(0.,0.,0.));
#14045=CARTESIAN_POINT('Origin',(0.375,0.5,0.));
#14046=CARTESIAN_POINT('',(-0.375,0.5,-4.59242549680257E-17));
#14047=CARTESIAN_POINT('Origin',(0.,0.5,0.));
#14048=CARTESIAN_POINT('Origin',(0.,0.475,0.));
#14049=CARTESIAN_POINT('',(-0.425,0.45,-5.20474889637625E-17));
#14050=CARTESIAN_POINT('Origin',(0.,0.45,0.));
#14051=CARTESIAN_POINT('',(-0.4,0.475,-4.89858719658941E-17));
#14052=CARTESIAN_POINT('Origin',(0.,0.24,0.));
#14053=CARTESIAN_POINT('',(-0.425,0.0299999999999998,-5.20474889637625E-17));
#14054=CARTESIAN_POINT('Origin',(0.,0.0299999999999998,0.));
#14055=CARTESIAN_POINT('',(-0.425,0.24,-5.20474889637625E-17));
#14056=CARTESIAN_POINT('Origin',(0.,0.0150000000000001,0.));
#14057=CARTESIAN_POINT('',(-0.395,4.85722573273506E-17,-4.83735485663204E-17));
#14058=CARTESIAN_POINT('Origin',(0.,0.,0.));
#14059=CARTESIAN_POINT('',(-0.41,0.0150000000000001,-5.02105187650415E-17));
#14060=CARTESIAN_POINT('Origin',(0.27,0.,0.));
#14061=CARTESIAN_POINT('',(-0.27,0.,-3.30654635769785E-17));
#14062=CARTESIAN_POINT('Origin',(0.,0.,0.));
#14063=CARTESIAN_POINT('Origin',(0.,-0.02,0.));
#14064=CARTESIAN_POINT('',(-0.24505,-0.0498999999999999,3.00099698131059E-17));
#14065=CARTESIAN_POINT('Origin',(0.,-0.0498999999999999,0.));
#14066=CARTESIAN_POINT('',(-0.26,-0.02,-3.18408167778312E-17));
#14067=CARTESIAN_POINT('Origin',(0.,-0.995,0.));
#14068=CARTESIAN_POINT('',(-0.24505,-1.95495,3.00099698131059E-17));
#14069=CARTESIAN_POINT('Origin',(0.,-1.95495,0.));
#14070=CARTESIAN_POINT('',(-0.24505,-0.995,-3.00099698131059E-17));
#14071=CARTESIAN_POINT('Origin',(0.,-1.975,0.));
#14072=CARTESIAN_POINT('',(-0.2,-2.,-2.44929359829471E-17));
#14073=CARTESIAN_POINT('Origin',(0.,-2.,0.));
#14074=CARTESIAN_POINT('',(-0.225,-1.975,-2.75545529808154E-17));
#14075=CARTESIAN_POINT('Origin',(0.,-2.,0.));
#14076=CARTESIAN_POINT('Origin',(0.115470053837925,-0.5,-0.2));
#14077=CARTESIAN_POINT('',(0.23094010767585,-0.5,0.));
#14078=CARTESIAN_POINT('',(0.115470053837925,-0.5,-0.2));
#14079=CARTESIAN_POINT('',(0.23094010767585,-0.5,0.));
#14080=CARTESIAN_POINT('',(0.115470053837925,-0.8,-0.2));
#14081=CARTESIAN_POINT('',(0.115470053837925,-0.5,-0.2));
#14082=CARTESIAN_POINT('',(0.23094010767585,-0.8,0.));
#14083=CARTESIAN_POINT('',(0.23094010767585,-0.8,0.));
#14084=CARTESIAN_POINT('',(0.23094010767585,-0.5,0.));
#14085=CARTESIAN_POINT('Origin',(-0.115470053837925,-0.5,-0.2));
#14086=CARTESIAN_POINT('',(-0.115470053837925,-0.5,-0.2));
#14087=CARTESIAN_POINT('',(0.115470053837925,-0.5,-0.2));
#14088=CARTESIAN_POINT('',(-0.115470053837925,-0.8,-0.2));
#14089=CARTESIAN_POINT('',(-0.115470053837925,-0.5,-0.2));
#14090=CARTESIAN_POINT('',(0.115470053837925,-0.8,-0.2));
#14091=CARTESIAN_POINT('Origin',(-0.23094010767585,-0.5,-2.77555756156289E-17));
#14092=CARTESIAN_POINT('',(-0.23094010767585,-0.5,-2.82820063659975E-17));
#14093=CARTESIAN_POINT('',(-0.115470053837925,-0.5,-0.2));
#14094=CARTESIAN_POINT('',(-0.23094010767585,-0.8,-2.77555756156289E-17));
#14095=CARTESIAN_POINT('',(-0.23094010767585,-0.5,-2.82820063659975E-17));
#14096=CARTESIAN_POINT('',(-0.115470053837925,-0.8,-0.2));
#14097=CARTESIAN_POINT('Origin',(-0.115470053837925,-0.5,0.2));
#14098=CARTESIAN_POINT('',(-0.115470053837925,-0.5,0.2));
#14099=CARTESIAN_POINT('',(-0.23094010767585,-0.5,-2.82820063659975E-17));
#14100=CARTESIAN_POINT('',(-0.115470053837925,-0.8,0.2));
#14101=CARTESIAN_POINT('',(-0.115470053837925,-0.5,0.2));
#14102=CARTESIAN_POINT('',(-0.23094010767585,-0.8,-2.82820063659975E-17));
#14103=CARTESIAN_POINT('Origin',(0.115470053837925,-0.5,0.2));
#14104=CARTESIAN_POINT('',(0.115470053837925,-0.5,0.2));
#14105=CARTESIAN_POINT('',(-0.115470053837925,-0.5,0.2));
#14106=CARTESIAN_POINT('',(0.115470053837925,-0.8,0.2));
#14107=CARTESIAN_POINT('',(0.115470053837925,-0.5,0.2));
#14108=CARTESIAN_POINT('',(-0.115470053837925,-0.8,0.2));
#14109=CARTESIAN_POINT('Origin',(0.23094010767585,-0.5,0.));
#14110=CARTESIAN_POINT('',(0.115470053837925,-0.5,0.2));
#14111=CARTESIAN_POINT('',(0.115470053837925,-0.8,0.2));
#14112=CARTESIAN_POINT('Origin',(0.,-0.5,0.));
#14113=CARTESIAN_POINT('Origin',(0.,-0.8,0.));
#14983=UNCERTAINTY_MEASURE_WITH_UNIT(LENGTH_MEASURE(0.001),#15041,
'DISTANCE_ACCURACY_VALUE',
'Maximum model space distance between geometric entities at asserted c
onnectivities');
#15000=UNCERTAINTY_MEASURE_WITH_UNIT(LENGTH_MEASURE(0.001),#15041,
'DISTANCE_ACCURACY_VALUE',
'Maximum model space distance between geometric entities at asserted c
onnectivities');
#15023=(
GEOMETRIC_REPRESENTATION_CONTEXT(3)
GLOBAL_UNCERTAINTY_ASSIGNED_CONTEXT((#14983))
GLOBAL_UNIT_ASSIGNED_CONTEXT((#15041,#15043,#15044))
REPRESENTATION_CONTEXT('','3D')
);
#15040=(
GEOMETRIC_REPRESENTATION_CONTEXT(3)
GLOBAL_UNCERTAINTY_ASSIGNED_CONTEXT((#15000))
GLOBAL_UNIT_ASSIGNED_CONTEXT((#15041,#15043,#15044))
REPRESENTATION_CONTEXT('','3D')
);
#15041=(
LENGTH_UNIT()
NAMED_UNIT(*)
SI_UNIT(.CENTI.,.METRE.)
);
#15043=(
NAMED_UNIT(*)
PLANE_ANGLE_UNIT()
SI_UNIT($,.RADIAN.)
);
#15044=(
NAMED_UNIT(*)
SI_UNIT($,.STERADIAN.)
SOLID_ANGLE_UNIT()
);
#15067=SHAPE_DEFINITION_REPRESENTATION(#15106,#15204);
#15106=PRODUCT_DEFINITION_SHAPE('',$,#15244);
#15204=SHAPE_REPRESENTATION('',(#7873),#15023);
#15221=PRODUCT_DEFINITION_CONTEXT('part definition',#15340,'design');
#15244=PRODUCT_DEFINITION('Cap Screw - M5x20','Cap Screw - M5x20',#15283,
#15221);
#15283=PRODUCT_DEFINITION_FORMATION('',$,#15364);
#15340=APPLICATION_CONTEXT(
'Core Data for Automotive Mechanical Design Process');
#15341=PRODUCT_CONTEXT('part definition',#15340,'mechanical');
#15364=PRODUCT('Cap Screw - M5x20','Cap Screw - M5x20',
'Cap Screw - M5x20',(#15341));
#15458=COLOUR_RGB('Black',0.12,0.14,0.17);
#15459=FILL_AREA_STYLE_COLOUR('',#15458);
#15460=FILL_AREA_STYLE('',(#15459));
#15461=SURFACE_STYLE_FILL_AREA(#15460);
#15462=SURFACE_SIDE_STYLE('',(#15461));
#15463=SURFACE_STYLE_USAGE(.BOTH.,#15462);
#15464=PRESENTATION_STYLE_ASSIGNMENT((#15463));
ENDSEC;
END-ISO-10303-21;
